ISO-10303-21;
HEADER;
/* Generated by software containing ST-Developer
 * from STEP Tools, Inc. (www.steptools.com) 
 */

FILE_DESCRIPTION(
/* description */ (
'Independent manual bench leaf bending machine,200mm work width. Fabri
cated welded frame and folding leaf, repeated bushed and fully retaine
d hinge hardware, two handles with bonded grips, beveled clamping beam
 and modeledM12 clamp screws.2mm omitted-workpiece assembly reference 
gap, not a capacity claim. Native135deg hinge travel. Weld sizing, pro
duction fits, material condition, bending capacity, strength and life 
unassigned.'),
/* implementation_level */ '2;1');

FILE_NAME(
/* name */ 'Flat washer M12.step',
/* time_stamp */ '2026-11-14T09:11:34-08:00',
/* author */ (''),
/* organization */ (''),
/* preprocessor_version */ 'ST-DEVELOPER v20.2',
/* originating_system */ 'Autodesk Translation Framework v15.17.0.0',
/* authorisation */ '');

FILE_SCHEMA (('AUTOMOTIVE_DESIGN { 1 0 10303 214 3 1 1 }'));
ENDSEC;

DATA;
#10=MECHANICAL_DESIGN_GEOMETRIC_PRESENTATION_REPRESENTATION('',(#453),#37701);
#417=SHAPE_REPRESENTATION_RELATIONSHIP('SRR','None',#37786,#435);
#435=ADVANCED_BREP_SHAPE_REPRESENTATION('',(#471),#37690);
#453=STYLED_ITEM('',(#37880),#471);
#471=MANIFOLD_SOLID_BREP('Body1',#4151);
#502=FACE_BOUND('',#920,.T.);
#503=FACE_BOUND('',#922,.T.);
#554=PLANE('',#4495);
#555=PLANE('',#4496);
#685=FACE_OUTER_BOUND('',#917,.T.);
#686=FACE_OUTER_BOUND('',#918,.T.);
#687=FACE_OUTER_BOUND('',#919,.T.);
#688=FACE_OUTER_BOUND('',#921,.T.);
#917=EDGE_LOOP('',(#3127,#3128,#3129,#3130));
#918=EDGE_LOOP('',(#3131,#3132,#3133,#3134));
#919=EDGE_LOOP('',(#3135));
#920=EDGE_LOOP('',(#3136));
#921=EDGE_LOOP('',(#3137));
#922=EDGE_LOOP('',(#3138));
#1173=LINE('',#14156,#1422);
#1174=LINE('',#14162,#1423);
#1422=VECTOR('',#5080,6.5);
#1423=VECTOR('',#5087,12.);
#1592=CIRCLE('',#4490,6.5);
#1593=CIRCLE('',#4491,6.5);
#1594=CIRCLE('',#4493,12.);
#1595=CIRCLE('',#4494,12.);
#1812=VERTEX_POINT('',#14153);
#1813=VERTEX_POINT('',#14155);
#1814=VERTEX_POINT('',#14159);
#1815=VERTEX_POINT('',#14161);
#2297=EDGE_CURVE('',#1812,#1812,#1592,.T.);
#2298=EDGE_CURVE('',#1812,#1813,#1173,.T.);
#2299=EDGE_CURVE('',#1813,#1813,#1593,.T.);
#2300=EDGE_CURVE('',#1814,#1814,#1594,.T.);
#2301=EDGE_CURVE('',#1814,#1815,#1174,.T.);
#2302=EDGE_CURVE('',#1815,#1815,#1595,.T.);
#3127=ORIENTED_EDGE('',*,*,#2297,.T.);
#3128=ORIENTED_EDGE('',*,*,#2298,.T.);
#3129=ORIENTED_EDGE('',*,*,#2299,.F.);
#3130=ORIENTED_EDGE('',*,*,#2298,.F.);
#3131=ORIENTED_EDGE('',*,*,#2300,.F.);
#3132=ORIENTED_EDGE('',*,*,#2301,.T.);
#3133=ORIENTED_EDGE('',*,*,#2302,.T.);
#3134=ORIENTED_EDGE('',*,*,#2301,.F.);
#3135=ORIENTED_EDGE('',*,*,#2300,.T.);
#3136=ORIENTED_EDGE('',*,*,#2299,.T.);
#3137=ORIENTED_EDGE('',*,*,#2302,.F.);
#3138=ORIENTED_EDGE('',*,*,#2297,.F.);
#3854=CYLINDRICAL_SURFACE('',#4489,6.5);
#3855=CYLINDRICAL_SURFACE('',#4492,12.);
#4015=ADVANCED_FACE('',(#685),#3854,.F.);
#4016=ADVANCED_FACE('',(#686),#3855,.T.);
#4017=ADVANCED_FACE('',(#687,#502),#554,.T.);
#4018=ADVANCED_FACE('',(#688,#503),#555,.F.);
#4151=CLOSED_SHELL('',(#4015,#4016,#4017,#4018));
#4488=AXIS2_PLACEMENT_3D('',#14151,#5074,#5075);
#4489=AXIS2_PLACEMENT_3D('',#14152,#5076,#5077);
#4490=AXIS2_PLACEMENT_3D('',#14154,#5078,#5079);
#4491=AXIS2_PLACEMENT_3D('',#14157,#5081,#5082);
#4492=AXIS2_PLACEMENT_3D('',#14158,#5083,#5084);
#4493=AXIS2_PLACEMENT_3D('',#14160,#5085,#5086);
#4494=AXIS2_PLACEMENT_3D('',#14163,#5088,#5089);
#4495=AXIS2_PLACEMENT_3D('',#14164,#5090,#5091);
#4496=AXIS2_PLACEMENT_3D('',#14165,#5092,#5093);
#5074=DIRECTION('axis',(0.,0.,1.));
#5075=DIRECTION('refdir',(1.,0.,0.));
#5076=DIRECTION('center_axis',(0.,0.,1.));
#5077=DIRECTION('ref_axis',(1.,0.,0.));
#5078=DIRECTION('center_axis',(0.,0.,-1.));
#5079=DIRECTION('ref_axis',(1.,0.,0.));
#5080=DIRECTION('',(0.,0.,1.));
#5081=DIRECTION('center_axis',(0.,0.,-1.));
#5082=DIRECTION('ref_axis',(1.,0.,0.));
#5083=DIRECTION('center_axis',(0.,0.,1.));
#5084=DIRECTION('ref_axis',(1.,0.,0.));
#5085=DIRECTION('center_axis',(0.,0.,1.));
#5086=DIRECTION('ref_axis',(1.,0.,0.));
#5087=DIRECTION('',(0.,0.,-1.));
#5088=DIRECTION('center_axis',(0.,0.,1.));
#5089=DIRECTION('ref_axis',(1.,0.,0.));
#5090=DIRECTION('center_axis',(0.,0.,1.));
#5091=DIRECTION('ref_axis',(1.,0.,0.));
#5092=DIRECTION('center_axis',(0.,0.,1.));
#5093=DIRECTION('ref_axis',(1.,0.,0.));
#14151=CARTESIAN_POINT('',(0.,0.,0.));
#14152=CARTESIAN_POINT('Origin',(0.,0.,0.));
#14153=CARTESIAN_POINT('',(-6.5,-7.9602041944578E-16,0.));
#14154=CARTESIAN_POINT('Origin',(0.,0.,0.));
#14155=CARTESIAN_POINT('',(-6.5,-7.9602041944578E-16,2.));
#14156=CARTESIAN_POINT('',(-6.5,-7.9602041944578E-16,0.));
#14157=CARTESIAN_POINT('Origin',(0.,0.,2.));
#14158=CARTESIAN_POINT('Origin',(0.,0.,0.));
#14159=CARTESIAN_POINT('',(-12.,-1.46957615897682E-15,2.));
#14160=CARTESIAN_POINT('Origin',(0.,0.,2.));
#14161=CARTESIAN_POINT('',(-12.,-1.46957615897682E-15,0.));
#14162=CARTESIAN_POINT('',(-12.,-1.46957615897682E-15,0.));
#14163=CARTESIAN_POINT('Origin',(0.,0.,0.));
#14164=CARTESIAN_POINT('Origin',(0.,0.,2.));
#14165=CARTESIAN_POINT('Origin',(0.,0.,0.));
#37670=UNCERTAINTY_MEASURE_WITH_UNIT(LENGTH_MEASURE(0.01),#37702,
'DISTANCE_ACCURACY_VALUE',
'Maximum model space distance between geometric entities at asserted c
onnectivities');
#37681=UNCERTAINTY_MEASURE_WITH_UNIT(LENGTH_MEASURE(0.01),#37702,
'DISTANCE_ACCURACY_VALUE',
'Maximum model space distance between geometric entities at asserted c
onnectivities');
#37690=(
GEOMETRIC_REPRESENTATION_CONTEXT(3)
GLOBAL_UNCERTAINTY_ASSIGNED_CONTEXT((#37670))
GLOBAL_UNIT_ASSIGNED_CONTEXT((#37702,#37704,#37705))
REPRESENTATION_CONTEXT('','3D')
);
#37701=(
GEOMETRIC_REPRESENTATION_CONTEXT(3)
GLOBAL_UNCERTAINTY_ASSIGNED_CONTEXT((#37681))
GLOBAL_UNIT_ASSIGNED_CONTEXT((#37702,#37704,#37705))
REPRESENTATION_CONTEXT('','3D')
);
#37702=(
LENGTH_UNIT()
NAMED_UNIT(*)
SI_UNIT(.MILLI.,.METRE.)
);
#37704=(
NAMED_UNIT(*)
PLANE_ANGLE_UNIT()
SI_UNIT($,.RADIAN.)
);
#37705=(
NAMED_UNIT(*)
SI_UNIT($,.STERADIAN.)
SOLID_ANGLE_UNIT()
);
#37714=SHAPE_DEFINITION_REPRESENTATION(#37733,#37786);
#37733=PRODUCT_DEFINITION_SHAPE('',$,#37806);
#37786=SHAPE_REPRESENTATION('',(#4488),#37690);
#37797=PRODUCT_DEFINITION_CONTEXT('part definition',#37856,'design');
#37806=PRODUCT_DEFINITION('Flat washer M12','Flat washer M12',#37825,#37797);
#37825=PRODUCT_DEFINITION_FORMATION('',$,#37866);
#37856=APPLICATION_CONTEXT(
'Core Data for Automotive Mechanical Design Process');
#37857=PRODUCT_CONTEXT('part definition',#37856,'mechanical');
#37866=PRODUCT('Flat washer M12','Flat washer M12',$,(#37857));
#37880=PRESENTATION_STYLE_ASSIGNMENT((#37888));
#37888=SURFACE_STYLE_USAGE(.BOTH.,#37896);
#37896=SURFACE_SIDE_STYLE('',(#37904));
#37904=SURFACE_STYLE_FILL_AREA(#37912);
#37912=FILL_AREA_STYLE('Opaque(185,192,202)',(#37920));
#37920=FILL_AREA_STYLE_COLOUR('Opaque(185,192,202)',#37928);
#37928=COLOUR_RGB('Opaque(185,192,202)',0.725490196078431,0.752941176470588,
0.792156862745098);
ENDSEC;
END-ISO-10303-21;
